ISO-10303-21;
HEADER;
FILE_DESCRIPTION((''),'2;1');
FILE_NAME('Hex_Screw_M8x35.step','2026-10-09T12:47:58-07:00',(''),(''),'','','');
FILE_SCHEMA (('AUTOMOTIVE_DESIGN { 1 0 10303 214 3 1 1 }'));
ENDSEC;
DATA;
#10=MECHANICAL_DESIGN_GEOMETRIC_PRESENTATION_REPRESENTATION('',(#321),#3475);
#11=(
BOUNDED_CURVE()
B_SPLINE_CURVE(2,(#3374,#3375,#3376),.UNSPECIFIED.,.F.,.F.)
B_SPLINE_CURVE_WITH_KNOTS((3,3),(-1.6071868741402,-0.951706480249473),
 .UNSPECIFIED.)
CURVE()
GEOMETRIC_REPRESENTATION_ITEM()
RATIONAL_B_SPLINE_CURVE((1.7594376617802,1.7594376617802,1.63311572113257))
REPRESENTATION_ITEM('')
) ;
#12=(
BOUNDED_CURVE()
B_SPLINE_CURVE(2,(#3377,#3378,#3379),.UNSPECIFIED.,.F.,.F.)
B_SPLINE_CURVE_WITH_KNOTS((3,3),(-2.26266726803093,-1.6071868741402),
 .UNSPECIFIED.)
CURVE()
GEOMETRIC_REPRESENTATION_ITEM()
RATIONAL_B_SPLINE_CURVE((1.63311572113257,1.7594376617802,1.7594376617802))
REPRESENTATION_ITEM('')
) ;
#13=(
BOUNDED_CURVE()
B_SPLINE_CURVE(2,(#3382,#3383,#3384),.UNSPECIFIED.,.F.,.F.)
B_SPLINE_CURVE_WITH_KNOTS((3,3),(-1.6071868741402,-0.951706480249475),
 .UNSPECIFIED.)
CURVE()
GEOMETRIC_REPRESENTATION_ITEM()
RATIONAL_B_SPLINE_CURVE((1.7594376617802,1.7594376617802,1.63311572113257))
REPRESENTATION_ITEM('')
) ;
#14=(
BOUNDED_CURVE()
B_SPLINE_CURVE(2,(#3385,#3386,#3387),.UNSPECIFIED.,.F.,.F.)
B_SPLINE_CURVE_WITH_KNOTS((3,3),(-2.26266726803093,-1.6071868741402),
 .UNSPECIFIED.)
CURVE()
GEOMETRIC_REPRESENTATION_ITEM()
RATIONAL_B_SPLINE_CURVE((1.63311572113257,1.7594376617802,1.7594376617802))
REPRESENTATION_ITEM('')
) ;
#15=(
BOUNDED_CURVE()
B_SPLINE_CURVE(2,(#3390,#3391,#3392),.UNSPECIFIED.,.F.,.F.)
B_SPLINE_CURVE_WITH_KNOTS((3,3),(-2.26266726803093,-1.6071868741402),
 .UNSPECIFIED.)
CURVE()
GEOMETRIC_REPRESENTATION_ITEM()
RATIONAL_B_SPLINE_CURVE((1.63311572113257,1.7594376617802,1.7594376617802))
REPRESENTATION_ITEM('')
) ;
#16=(
BOUNDED_CURVE()
B_SPLINE_CURVE(2,(#3393,#3394,#3395),.UNSPECIFIED.,.F.,.F.)
B_SPLINE_CURVE_WITH_KNOTS((3,3),(-1.6071868741402,-0.951706480249475),
 .UNSPECIFIED.)
CURVE()
GEOMETRIC_REPRESENTATION_ITEM()
RATIONAL_B_SPLINE_CURVE((1.7594376617802,1.7594376617802,1.63311572113257))
REPRESENTATION_ITEM('')
) ;
#17=(
BOUNDED_CURVE()
B_SPLINE_CURVE(2,(#3398,#3399,#3400),.UNSPECIFIED.,.F.,.F.)
B_SPLINE_CURVE_WITH_KNOTS((3,3),(-2.26266726803093,-1.6071868741402),
 .UNSPECIFIED.)
CURVE()
GEOMETRIC_REPRESENTATION_ITEM()
RATIONAL_B_SPLINE_CURVE((1.63311572113257,1.7594376617802,1.7594376617802))
REPRESENTATION_ITEM('')
) ;
#18=(
BOUNDED_CURVE()
B_SPLINE_CURVE(2,(#3401,#3402,#3403),.UNSPECIFIED.,.F.,.F.)
B_SPLINE_CURVE_WITH_KNOTS((3,3),(-1.6071868741402,-0.951706480249475),
 .UNSPECIFIED.)
CURVE()
GEOMETRIC_REPRESENTATION_ITEM()
RATIONAL_B_SPLINE_CURVE((1.7594376617802,1.7594376617802,1.63311572113257))
REPRESENTATION_ITEM('')
) ;
#19=(
BOUNDED_CURVE()
B_SPLINE_CURVE(2,(#3406,#3407,#3408),.UNSPECIFIED.,.F.,.F.)
B_SPLINE_CURVE_WITH_KNOTS((3,3),(-1.6071868741402,-0.951706480249475),
 .UNSPECIFIED.)
CURVE()
GEOMETRIC_REPRESENTATION_ITEM()
RATIONAL_B_SPLINE_CURVE((1.7594376617802,1.7594376617802,1.63311572113257))
REPRESENTATION_ITEM('')
) ;
#20=(
BOUNDED_CURVE()
B_SPLINE_CURVE(2,(#3409,#3410,#3411),.UNSPECIFIED.,.F.,.F.)
B_SPLINE_CURVE_WITH_KNOTS((3,3),(-2.26266726803093,-1.6071868741402),
 .UNSPECIFIED.)
CURVE()
GEOMETRIC_REPRESENTATION_ITEM()
RATIONAL_B_SPLINE_CURVE((1.63311572113258,1.7594376617802,1.7594376617802))
REPRESENTATION_ITEM('')
) ;
#21=(
BOUNDED_CURVE()
B_SPLINE_CURVE(2,(#3414,#3415,#3416),.UNSPECIFIED.,.F.,.F.)
B_SPLINE_CURVE_WITH_KNOTS((3,3),(-2.26266726803093,-1.6071868741402),
 .UNSPECIFIED.)
CURVE()
GEOMETRIC_REPRESENTATION_ITEM()
RATIONAL_B_SPLINE_CURVE((1.63311572113257,1.7594376617802,1.7594376617802))
REPRESENTATION_ITEM('')
) ;
#22=(
BOUNDED_CURVE()
B_SPLINE_CURVE(2,(#3417,#3418,#3419),.UNSPECIFIED.,.F.,.F.)
B_SPLINE_CURVE_WITH_KNOTS((3,3),(-1.6071868741402,-0.951706480249472),
 .UNSPECIFIED.)
CURVE()
GEOMETRIC_REPRESENTATION_ITEM()
RATIONAL_B_SPLINE_CURVE((1.7594376617802,1.7594376617802,1.63311572113257))
REPRESENTATION_ITEM('')
) ;
#30=TOROIDAL_SURFACE('',#2162,4.4,0.4) ;
#34=CONICAL_SURFACE('',#2175,3.3095,0.785398163397441) ;
#35=CONICAL_SURFACE('',#2194,6.5,1.0471975511966) ;
#36=CONICAL_SURFACE('',#2195,6.5,1.0471975511966) ;
#37=CONICAL_SURFACE('',#2196,6.5,1.0471975511966) ;
#38=CONICAL_SURFACE('',#2197,6.5,1.0471975511966) ;
#39=CONICAL_SURFACE('',#2198,6.5,1.0471975511966) ;
#40=CONICAL_SURFACE('',#2199,6.5,1.0471975511966) ;
#165=FACE_BOUND('',#566,.T.) ;
#237=CIRCLE('',#2163,4.) ;
#238=CIRCLE('',#2164,4.) ;
#239=CIRCLE('',#2165,0.4) ;
#240=CIRCLE('',#2166,4.4) ;
#241=CIRCLE('',#2168,6.5) ;
#242=CIRCLE('',#2169,6.5) ;
#243=CIRCLE('',#2170,6.5) ;
#244=CIRCLE('',#2171,6.5) ;
#245=CIRCLE('',#2172,6.5) ;
#246=CIRCLE('',#2173,6.5) ;
#247=CIRCLE('',#2174,6.5) ;
#248=CIRCLE('',#2176,4.) ;
#249=CIRCLE('',#2177,3.3095) ;
#250=CIRCLE('',#2188,6.5) ;
#251=CIRCLE('',#2189,6.5) ;
#252=CIRCLE('',#2190,6.5) ;
#253=CIRCLE('',#2191,6.5) ;
#254=CIRCLE('',#2192,6.5) ;
#255=CIRCLE('',#2193,6.5) ;
#284=CYLINDRICAL_SURFACE('',#2167,6.5) ;
#285=CYLINDRICAL_SURFACE('',#2178,4.) ;
#297=SHAPE_REPRESENTATION_RELATIONSHIP('SRR','None',#3554,#309) ;
#309=ADVANCED_BREP_SHAPE_REPRESENTATION('',(#333),#3474) ;
#321=STYLED_ITEM('',(#3628),#333) ;
#333=MANIFOLD_SOLID_BREP('Body1',#1835) ;
#423=FACE_OUTER_BOUND('',#561,.T.) ;
#424=FACE_OUTER_BOUND('',#562,.T.) ;
#425=FACE_OUTER_BOUND('',#563,.T.) ;
#426=FACE_OUTER_BOUND('',#564,.T.) ;
#427=FACE_OUTER_BOUND('',#565,.T.) ;
#428=FACE_OUTER_BOUND('',#567,.T.) ;
#429=FACE_OUTER_BOUND('',#568,.T.) ;
#430=FACE_OUTER_BOUND('',#569,.T.) ;
#431=FACE_OUTER_BOUND('',#570,.T.) ;
#432=FACE_OUTER_BOUND('',#571,.T.) ;
#433=FACE_OUTER_BOUND('',#572,.T.) ;
#434=FACE_OUTER_BOUND('',#573,.T.) ;
#435=FACE_OUTER_BOUND('',#574,.T.) ;
#436=FACE_OUTER_BOUND('',#575,.T.) ;
#437=FACE_OUTER_BOUND('',#576,.T.) ;
#438=FACE_OUTER_BOUND('',#577,.T.) ;
#439=FACE_OUTER_BOUND('',#578,.T.) ;
#440=FACE_OUTER_BOUND('',#579,.T.) ;
#441=FACE_OUTER_BOUND('',#580,.T.) ;
#442=FACE_OUTER_BOUND('',#581,.T.) ;
#443=FACE_OUTER_BOUND('',#582,.T.) ;
#444=FACE_OUTER_BOUND('',#583,.T.) ;
#445=FACE_OUTER_BOUND('',#584,.T.) ;
#446=FACE_OUTER_BOUND('',#585,.T.) ;
#447=FACE_OUTER_BOUND('',#586,.T.) ;
#561=EDGE_LOOP('',(#1540,#1541,#1542,#1543,#1544)) ;
#562=EDGE_LOOP('',(#1545,#1546,#1547,#1548,#1549,#1550,#1551,#1552,#1553)) ;
#563=EDGE_LOOP('',(#1554,#1555,#1556,#1557)) ;
#564=EDGE_LOOP('',(#1558,#1559,#1560,#1561,#1562)) ;
#565=EDGE_LOOP('',(#1563)) ;
#566=EDGE_LOOP('',(#1564)) ;
#567=EDGE_LOOP('',(#1565)) ;
#568=EDGE_LOOP('',(#1566,#1567,#1568)) ;
#569=EDGE_LOOP('',(#1569,#1570,#1571)) ;
#570=EDGE_LOOP('',(#1572,#1573,#1574)) ;
#571=EDGE_LOOP('',(#1575,#1576,#1577)) ;
#572=EDGE_LOOP('',(#1578,#1579,#1580)) ;
#573=EDGE_LOOP('',(#1581,#1582,#1583)) ;
#574=EDGE_LOOP('',(#1584,#1585,#1586,#1587,#1588,#1589)) ;
#575=EDGE_LOOP('',(#1590,#1591,#1592)) ;
#576=EDGE_LOOP('',(#1593,#1594,#1595)) ;
#577=EDGE_LOOP('',(#1596,#1597,#1598)) ;
#578=EDGE_LOOP('',(#1599,#1600,#1601)) ;
#579=EDGE_LOOP('',(#1602,#1603,#1604)) ;
#580=EDGE_LOOP('',(#1605,#1606,#1607)) ;
#581=EDGE_LOOP('',(#1608,#1609,#1610,#1611,#1612,#1613)) ;
#582=EDGE_LOOP('',(#1614,#1615,#1616,#1617,#1618,#1619)) ;
#583=EDGE_LOOP('',(#1620,#1621,#1622,#1623,#1624,#1625)) ;
#584=EDGE_LOOP('',(#1626,#1627,#1628,#1629,#1630,#1631)) ;
#585=EDGE_LOOP('',(#1632,#1633,#1634,#1635,#1636,#1637)) ;
#586=EDGE_LOOP('',(#1638,#1639,#1640,#1641,#1642,#1643)) ;
#685=LINE('',#3323,#804) ;
#686=LINE('',#3329,#805) ;
#687=LINE('',#3332,#806) ;
#688=LINE('',#3337,#807) ;
#689=LINE('',#3338,#808) ;
#690=LINE('',#3341,#809) ;
#691=LINE('',#3342,#810) ;
#692=LINE('',#3345,#811) ;
#693=LINE('',#3346,#812) ;
#694=LINE('',#3349,#813) ;
#695=LINE('',#3350,#814) ;
#696=LINE('',#3353,#815) ;
#697=LINE('',#3354,#816) ;
#698=LINE('',#3357,#817) ;
#699=LINE('',#3358,#818) ;
#700=LINE('',#3421,#819) ;
#701=LINE('',#3422,#820) ;
#702=LINE('',#3424,#821) ;
#703=LINE('',#3426,#822) ;
#704=LINE('',#3428,#823) ;
#705=LINE('',#3430,#824) ;
#804=VECTOR('',#2722,6.5) ;
#805=VECTOR('',#2729,3.3095) ;
#806=VECTOR('',#2734,4.) ;
#807=VECTOR('',#2741,1000.) ;
#808=VECTOR('',#2742,1000.) ;
#809=VECTOR('',#2745,1000.) ;
#810=VECTOR('',#2746,1000.) ;
#811=VECTOR('',#2749,1000.) ;
#812=VECTOR('',#2750,1000.) ;
#813=VECTOR('',#2753,1000.) ;
#814=VECTOR('',#2754,1000.) ;
#815=VECTOR('',#2757,1000.) ;
#816=VECTOR('',#2758,1000.) ;
#817=VECTOR('',#2761,1000.) ;
#818=VECTOR('',#2762,1000.) ;
#819=VECTOR('',#2791,1000.) ;
#820=VECTOR('',#2792,1000.) ;
#821=VECTOR('',#2795,1000.) ;
#822=VECTOR('',#2798,1000.) ;
#823=VECTOR('',#2801,1000.) ;
#824=VECTOR('',#2804,1000.) ;
#939=VERTEX_POINT('',#3302) ;
#940=VERTEX_POINT('',#3303) ;
#941=VERTEX_POINT('',#3306) ;
#942=VERTEX_POINT('',#3310) ;
#943=VERTEX_POINT('',#3311) ;
#944=VERTEX_POINT('',#3313) ;
#945=VERTEX_POINT('',#3315) ;
#946=VERTEX_POINT('',#3317) ;
#947=VERTEX_POINT('',#3319) ;
#948=VERTEX_POINT('',#3322) ;
#949=VERTEX_POINT('',#3326) ;
#950=VERTEX_POINT('',#3328) ;
#951=VERTEX_POINT('',#3336) ;
#952=VERTEX_POINT('',#3340) ;
#953=VERTEX_POINT('',#3344) ;
#954=VERTEX_POINT('',#3348) ;
#955=VERTEX_POINT('',#3352) ;
#956=VERTEX_POINT('',#3356) ;
#957=VERTEX_POINT('',#3360) ;
#958=VERTEX_POINT('',#3361) ;
#959=VERTEX_POINT('',#3363) ;
#960=VERTEX_POINT('',#3365) ;
#961=VERTEX_POINT('',#3367) ;
#962=VERTEX_POINT('',#3369) ;
#963=VERTEX_POINT('',#3373) ;
#964=VERTEX_POINT('',#3381) ;
#965=VERTEX_POINT('',#3389) ;
#966=VERTEX_POINT('',#3397) ;
#967=VERTEX_POINT('',#3405) ;
#968=VERTEX_POINT('',#3413) ;
#1142=EDGE_CURVE('',#939,#940,#237,.T.) ;
#1143=EDGE_CURVE('',#940,#939,#238,.T.) ;
#1144=EDGE_CURVE('',#940,#941,#239,.T.) ;
#1145=EDGE_CURVE('',#941,#941,#240,.T.) ;
#1146=EDGE_CURVE('',#942,#943,#241,.T.) ;
#1147=EDGE_CURVE('',#944,#942,#242,.T.) ;
#1148=EDGE_CURVE('',#945,#944,#243,.T.) ;
#1149=EDGE_CURVE('',#946,#945,#244,.T.) ;
#1150=EDGE_CURVE('',#947,#946,#245,.T.) ;
#1151=EDGE_CURVE('',#943,#947,#246,.T.) ;
#1152=EDGE_CURVE('',#943,#948,#685,.T.) ;
#1153=EDGE_CURVE('',#948,#948,#247,.T.) ;
#1154=EDGE_CURVE('',#949,#949,#248,.T.) ;
#1155=EDGE_CURVE('',#949,#950,#686,.T.) ;
#1156=EDGE_CURVE('',#950,#950,#249,.T.) ;
#1157=EDGE_CURVE('',#939,#949,#687,.T.) ;
#1158=EDGE_CURVE('',#951,#942,#688,.T.) ;
#1159=EDGE_CURVE('',#943,#951,#689,.T.) ;
#1160=EDGE_CURVE('',#942,#952,#690,.T.) ;
#1161=EDGE_CURVE('',#952,#944,#691,.T.) ;
#1162=EDGE_CURVE('',#944,#953,#692,.T.) ;
#1163=EDGE_CURVE('',#953,#945,#693,.T.) ;
#1164=EDGE_CURVE('',#945,#954,#694,.T.) ;
#1165=EDGE_CURVE('',#954,#946,#695,.T.) ;
#1166=EDGE_CURVE('',#946,#955,#696,.T.) ;
#1167=EDGE_CURVE('',#955,#947,#697,.T.) ;
#1168=EDGE_CURVE('',#947,#956,#698,.T.) ;
#1169=EDGE_CURVE('',#956,#943,#699,.T.) ;
#1170=EDGE_CURVE('',#957,#958,#250,.T.) ;
#1171=EDGE_CURVE('',#959,#957,#251,.T.) ;
#1172=EDGE_CURVE('',#960,#959,#252,.T.) ;
#1173=EDGE_CURVE('',#961,#960,#253,.T.) ;
#1174=EDGE_CURVE('',#961,#962,#254,.T.) ;
#1175=EDGE_CURVE('',#958,#962,#255,.T.) ;
#1176=EDGE_CURVE('',#962,#963,#11,.T.) ;
#1177=EDGE_CURVE('',#963,#958,#12,.T.) ;
#1178=EDGE_CURVE('',#961,#964,#13,.T.) ;
#1179=EDGE_CURVE('',#964,#962,#14,.T.) ;
#1180=EDGE_CURVE('',#965,#961,#15,.T.) ;
#1181=EDGE_CURVE('',#960,#965,#16,.T.) ;
#1182=EDGE_CURVE('',#966,#960,#17,.T.) ;
#1183=EDGE_CURVE('',#959,#966,#18,.T.) ;
#1184=EDGE_CURVE('',#958,#967,#19,.T.) ;
#1185=EDGE_CURVE('',#967,#957,#20,.T.) ;
#1186=EDGE_CURVE('',#968,#959,#21,.T.) ;
#1187=EDGE_CURVE('',#957,#968,#22,.T.) ;
#1188=EDGE_CURVE('',#956,#968,#700,.T.) ;
#1189=EDGE_CURVE('',#951,#967,#701,.T.) ;
#1190=EDGE_CURVE('',#955,#966,#702,.T.) ;
#1191=EDGE_CURVE('',#954,#965,#703,.T.) ;
#1192=EDGE_CURVE('',#953,#964,#704,.T.) ;
#1193=EDGE_CURVE('',#952,#963,#705,.T.) ;
#1540=ORIENTED_EDGE('',*,*,#1142,.F.) ;
#1541=ORIENTED_EDGE('',*,*,#1143,.F.) ;
#1542=ORIENTED_EDGE('',*,*,#1144,.T.) ;
#1543=ORIENTED_EDGE('',*,*,#1145,.F.) ;
#1544=ORIENTED_EDGE('',*,*,#1144,.F.) ;
#1545=ORIENTED_EDGE('',*,*,#1146,.F.) ;
#1546=ORIENTED_EDGE('',*,*,#1147,.F.) ;
#1547=ORIENTED_EDGE('',*,*,#1148,.F.) ;
#1548=ORIENTED_EDGE('',*,*,#1149,.F.) ;
#1549=ORIENTED_EDGE('',*,*,#1150,.F.) ;
#1550=ORIENTED_EDGE('',*,*,#1151,.F.) ;
#1551=ORIENTED_EDGE('',*,*,#1152,.T.) ;
#1552=ORIENTED_EDGE('',*,*,#1153,.F.) ;
#1553=ORIENTED_EDGE('',*,*,#1152,.F.) ;
#1554=ORIENTED_EDGE('',*,*,#1154,.F.) ;
#1555=ORIENTED_EDGE('',*,*,#1155,.T.) ;
#1556=ORIENTED_EDGE('',*,*,#1156,.T.) ;
#1557=ORIENTED_EDGE('',*,*,#1155,.F.) ;
#1558=ORIENTED_EDGE('',*,*,#1142,.T.) ;
#1559=ORIENTED_EDGE('',*,*,#1143,.T.) ;
#1560=ORIENTED_EDGE('',*,*,#1157,.T.) ;
#1561=ORIENTED_EDGE('',*,*,#1154,.T.) ;
#1562=ORIENTED_EDGE('',*,*,#1157,.F.) ;
#1563=ORIENTED_EDGE('',*,*,#1153,.T.) ;
#1564=ORIENTED_EDGE('',*,*,#1145,.T.) ;
#1565=ORIENTED_EDGE('',*,*,#1156,.F.) ;
#1566=ORIENTED_EDGE('',*,*,#1158,.T.) ;
#1567=ORIENTED_EDGE('',*,*,#1146,.T.) ;
#1568=ORIENTED_EDGE('',*,*,#1159,.T.) ;
#1569=ORIENTED_EDGE('',*,*,#1160,.T.) ;
#1570=ORIENTED_EDGE('',*,*,#1161,.T.) ;
#1571=ORIENTED_EDGE('',*,*,#1147,.T.) ;
#1572=ORIENTED_EDGE('',*,*,#1162,.T.) ;
#1573=ORIENTED_EDGE('',*,*,#1163,.T.) ;
#1574=ORIENTED_EDGE('',*,*,#1148,.T.) ;
#1575=ORIENTED_EDGE('',*,*,#1164,.T.) ;
#1576=ORIENTED_EDGE('',*,*,#1165,.T.) ;
#1577=ORIENTED_EDGE('',*,*,#1149,.T.) ;
#1578=ORIENTED_EDGE('',*,*,#1166,.T.) ;
#1579=ORIENTED_EDGE('',*,*,#1167,.T.) ;
#1580=ORIENTED_EDGE('',*,*,#1150,.T.) ;
#1581=ORIENTED_EDGE('',*,*,#1168,.T.) ;
#1582=ORIENTED_EDGE('',*,*,#1169,.T.) ;
#1583=ORIENTED_EDGE('',*,*,#1151,.T.) ;
#1584=ORIENTED_EDGE('',*,*,#1170,.F.) ;
#1585=ORIENTED_EDGE('',*,*,#1171,.F.) ;
#1586=ORIENTED_EDGE('',*,*,#1172,.F.) ;
#1587=ORIENTED_EDGE('',*,*,#1173,.F.) ;
#1588=ORIENTED_EDGE('',*,*,#1174,.T.) ;
#1589=ORIENTED_EDGE('',*,*,#1175,.F.) ;
#1590=ORIENTED_EDGE('',*,*,#1176,.T.) ;
#1591=ORIENTED_EDGE('',*,*,#1177,.T.) ;
#1592=ORIENTED_EDGE('',*,*,#1175,.T.) ;
#1593=ORIENTED_EDGE('',*,*,#1178,.T.) ;
#1594=ORIENTED_EDGE('',*,*,#1179,.T.) ;
#1595=ORIENTED_EDGE('',*,*,#1174,.F.) ;
#1596=ORIENTED_EDGE('',*,*,#1180,.T.) ;
#1597=ORIENTED_EDGE('',*,*,#1173,.T.) ;
#1598=ORIENTED_EDGE('',*,*,#1181,.T.) ;
#1599=ORIENTED_EDGE('',*,*,#1182,.T.) ;
#1600=ORIENTED_EDGE('',*,*,#1172,.T.) ;
#1601=ORIENTED_EDGE('',*,*,#1183,.T.) ;
#1602=ORIENTED_EDGE('',*,*,#1184,.T.) ;
#1603=ORIENTED_EDGE('',*,*,#1185,.T.) ;
#1604=ORIENTED_EDGE('',*,*,#1170,.T.) ;
#1605=ORIENTED_EDGE('',*,*,#1186,.T.) ;
#1606=ORIENTED_EDGE('',*,*,#1171,.T.) ;
#1607=ORIENTED_EDGE('',*,*,#1187,.T.) ;
#1608=ORIENTED_EDGE('',*,*,#1169,.F.) ;
#1609=ORIENTED_EDGE('',*,*,#1188,.T.) ;
#1610=ORIENTED_EDGE('',*,*,#1187,.F.) ;
#1611=ORIENTED_EDGE('',*,*,#1185,.F.) ;
#1612=ORIENTED_EDGE('',*,*,#1189,.F.) ;
#1613=ORIENTED_EDGE('',*,*,#1159,.F.) ;
#1614=ORIENTED_EDGE('',*,*,#1167,.F.) ;
#1615=ORIENTED_EDGE('',*,*,#1190,.T.) ;
#1616=ORIENTED_EDGE('',*,*,#1183,.F.) ;
#1617=ORIENTED_EDGE('',*,*,#1186,.F.) ;
#1618=ORIENTED_EDGE('',*,*,#1188,.F.) ;
#1619=ORIENTED_EDGE('',*,*,#1168,.F.) ;
#1620=ORIENTED_EDGE('',*,*,#1165,.F.) ;
#1621=ORIENTED_EDGE('',*,*,#1191,.T.) ;
#1622=ORIENTED_EDGE('',*,*,#1181,.F.) ;
#1623=ORIENTED_EDGE('',*,*,#1182,.F.) ;
#1624=ORIENTED_EDGE('',*,*,#1190,.F.) ;
#1625=ORIENTED_EDGE('',*,*,#1166,.F.) ;
#1626=ORIENTED_EDGE('',*,*,#1163,.F.) ;
#1627=ORIENTED_EDGE('',*,*,#1192,.T.) ;
#1628=ORIENTED_EDGE('',*,*,#1178,.F.) ;
#1629=ORIENTED_EDGE('',*,*,#1180,.F.) ;
#1630=ORIENTED_EDGE('',*,*,#1191,.F.) ;
#1631=ORIENTED_EDGE('',*,*,#1164,.F.) ;
#1632=ORIENTED_EDGE('',*,*,#1161,.F.) ;
#1633=ORIENTED_EDGE('',*,*,#1193,.T.) ;
#1634=ORIENTED_EDGE('',*,*,#1176,.F.) ;
#1635=ORIENTED_EDGE('',*,*,#1179,.F.) ;
#1636=ORIENTED_EDGE('',*,*,#1192,.F.) ;
#1637=ORIENTED_EDGE('',*,*,#1162,.F.) ;
#1638=ORIENTED_EDGE('',*,*,#1158,.F.) ;
#1639=ORIENTED_EDGE('',*,*,#1189,.T.) ;
#1640=ORIENTED_EDGE('',*,*,#1184,.F.) ;
#1641=ORIENTED_EDGE('',*,*,#1177,.F.) ;
#1642=ORIENTED_EDGE('',*,*,#1193,.F.) ;
#1643=ORIENTED_EDGE('',*,*,#1160,.F.) ;
#1695=PLANE('',#2179) ;
#1696=PLANE('',#2180) ;
#1697=PLANE('',#2181) ;
#1698=PLANE('',#2182) ;
#1699=PLANE('',#2183) ;
#1700=PLANE('',#2184) ;
#1701=PLANE('',#2185) ;
#1702=PLANE('',#2186) ;
#1703=PLANE('',#2187) ;
#1704=PLANE('',#2200) ;
#1705=PLANE('',#2201) ;
#1706=PLANE('',#2202) ;
#1707=PLANE('',#2203) ;
#1708=PLANE('',#2204) ;
#1709=PLANE('',#2205) ;
#1799=ADVANCED_FACE('',(#423),#30,.F.) ;
#1800=ADVANCED_FACE('',(#424),#284,.T.) ;
#1801=ADVANCED_FACE('',(#425),#34,.T.) ;
#1802=ADVANCED_FACE('',(#426),#285,.T.) ;
#1803=ADVANCED_FACE('',(#427,#165),#1695,.T.) ;
#1804=ADVANCED_FACE('',(#428),#1696,.F.) ;
#1805=ADVANCED_FACE('',(#429),#1697,.T.) ;
#1806=ADVANCED_FACE('',(#430),#1698,.T.) ;
#1807=ADVANCED_FACE('',(#431),#1699,.T.) ;
#1808=ADVANCED_FACE('',(#432),#1700,.T.) ;
#1809=ADVANCED_FACE('',(#433),#1701,.T.) ;
#1810=ADVANCED_FACE('',(#434),#1702,.T.) ;
#1811=ADVANCED_FACE('',(#435),#1703,.F.) ;
#1812=ADVANCED_FACE('',(#436),#35,.T.) ;
#1813=ADVANCED_FACE('',(#437),#36,.T.) ;
#1814=ADVANCED_FACE('',(#438),#37,.T.) ;
#1815=ADVANCED_FACE('',(#439),#38,.T.) ;
#1816=ADVANCED_FACE('',(#440),#39,.T.) ;
#1817=ADVANCED_FACE('',(#441),#40,.T.) ;
#1818=ADVANCED_FACE('',(#442),#1704,.F.) ;
#1819=ADVANCED_FACE('',(#443),#1705,.F.) ;
#1820=ADVANCED_FACE('',(#444),#1706,.F.) ;
#1821=ADVANCED_FACE('',(#445),#1707,.F.) ;
#1822=ADVANCED_FACE('',(#446),#1708,.F.) ;
#1823=ADVANCED_FACE('',(#447),#1709,.F.) ;
#1835=CLOSED_SHELL('',(#1799,#1800,#1801,#1802,#1803,#1804,#1805,#1806,
#1807,#1808,#1809,#1810,#1811,#1812,#1813,#1814,#1815,#1816,#1817,#1818,
#1819,#1820,#1821,#1822,#1823)) ;
#2161=AXIS2_PLACEMENT_3D('',#3300,#2696,#2697) ;
#2162=AXIS2_PLACEMENT_3D('',#3301,#2698,#2699) ;
#2163=AXIS2_PLACEMENT_3D('',#3304,#2700,#2701) ;
#2164=AXIS2_PLACEMENT_3D('',#3305,#2702,#2703) ;
#2165=AXIS2_PLACEMENT_3D('',#3307,#2704,#2705) ;
#2166=AXIS2_PLACEMENT_3D('',#3308,#2706,#2707) ;
#2167=AXIS2_PLACEMENT_3D('',#3309,#2708,#2709) ;
#2168=AXIS2_PLACEMENT_3D('',#3312,#2710,#2711) ;
#2169=AXIS2_PLACEMENT_3D('',#3314,#2712,#2713) ;
#2170=AXIS2_PLACEMENT_3D('',#3316,#2714,#2715) ;
#2171=AXIS2_PLACEMENT_3D('',#3318,#2716,#2717) ;
#2172=AXIS2_PLACEMENT_3D('',#3320,#2718,#2719) ;
#2173=AXIS2_PLACEMENT_3D('',#3321,#2720,#2721) ;
#2174=AXIS2_PLACEMENT_3D('',#3324,#2723,#2724) ;
#2175=AXIS2_PLACEMENT_3D('',#3325,#2725,#2726) ;
#2176=AXIS2_PLACEMENT_3D('',#3327,#2727,#2728) ;
#2177=AXIS2_PLACEMENT_3D('',#3330,#2730,#2731) ;
#2178=AXIS2_PLACEMENT_3D('',#3331,#2732,#2733) ;
#2179=AXIS2_PLACEMENT_3D('',#3333,#2735,#2736) ;
#2180=AXIS2_PLACEMENT_3D('',#3334,#2737,#2738) ;
#2181=AXIS2_PLACEMENT_3D('',#3335,#2739,#2740) ;
#2182=AXIS2_PLACEMENT_3D('',#3339,#2743,#2744) ;
#2183=AXIS2_PLACEMENT_3D('',#3343,#2747,#2748) ;
#2184=AXIS2_PLACEMENT_3D('',#3347,#2751,#2752) ;
#2185=AXIS2_PLACEMENT_3D('',#3351,#2755,#2756) ;
#2186=AXIS2_PLACEMENT_3D('',#3355,#2759,#2760) ;
#2187=AXIS2_PLACEMENT_3D('',#3359,#2763,#2764) ;
#2188=AXIS2_PLACEMENT_3D('',#3362,#2765,#2766) ;
#2189=AXIS2_PLACEMENT_3D('',#3364,#2767,#2768) ;
#2190=AXIS2_PLACEMENT_3D('',#3366,#2769,#2770) ;
#2191=AXIS2_PLACEMENT_3D('',#3368,#2771,#2772) ;
#2192=AXIS2_PLACEMENT_3D('',#3370,#2773,#2774) ;
#2193=AXIS2_PLACEMENT_3D('',#3371,#2775,#2776) ;
#2194=AXIS2_PLACEMENT_3D('',#3372,#2777,#2778) ;
#2195=AXIS2_PLACEMENT_3D('',#3380,#2779,#2780) ;
#2196=AXIS2_PLACEMENT_3D('',#3388,#2781,#2782) ;
#2197=AXIS2_PLACEMENT_3D('',#3396,#2783,#2784) ;
#2198=AXIS2_PLACEMENT_3D('',#3404,#2785,#2786) ;
#2199=AXIS2_PLACEMENT_3D('',#3412,#2787,#2788) ;
#2200=AXIS2_PLACEMENT_3D('',#3420,#2789,#2790) ;
#2201=AXIS2_PLACEMENT_3D('',#3423,#2793,#2794) ;
#2202=AXIS2_PLACEMENT_3D('',#3425,#2796,#2797) ;
#2203=AXIS2_PLACEMENT_3D('',#3427,#2799,#2800) ;
#2204=AXIS2_PLACEMENT_3D('',#3429,#2802,#2803) ;
#2205=AXIS2_PLACEMENT_3D('',#3431,#2805,#2806) ;
#2696=DIRECTION('axis',(0.,0.,1.)) ;
#2697=DIRECTION('refdir',(1.,0.,0.)) ;
#2698=DIRECTION('center_axis',(1.,0.,0.)) ;
#2699=DIRECTION('ref_axis',(0.,0.,-1.)) ;
#2700=DIRECTION('center_axis',(1.,0.,0.)) ;
#2701=DIRECTION('ref_axis',(0.,0.,-1.)) ;
#2702=DIRECTION('center_axis',(1.,0.,0.)) ;
#2703=DIRECTION('ref_axis',(0.,0.,-1.)) ;
#2704=DIRECTION('center_axis',(0.,1.,1.22464679914735E-16)) ;
#2705=DIRECTION('ref_axis',(0.,-1.22464679914735E-16,1.)) ;
#2706=DIRECTION('center_axis',(-1.,0.,0.)) ;
#2707=DIRECTION('ref_axis',(0.,0.,-1.)) ;
#2708=DIRECTION('center_axis',(-1.,0.,0.)) ;
#2709=DIRECTION('ref_axis',(0.,0.,1.)) ;
#2710=DIRECTION('center_axis',(-1.,0.,0.)) ;
#2711=DIRECTION('ref_axis',(0.,0.,1.)) ;
#2712=DIRECTION('center_axis',(-1.,0.,0.)) ;
#2713=DIRECTION('ref_axis',(0.,0.,1.)) ;
#2714=DIRECTION('center_axis',(-1.,0.,0.)) ;
#2715=DIRECTION('ref_axis',(0.,0.,1.)) ;
#2716=DIRECTION('center_axis',(-1.,0.,0.)) ;
#2717=DIRECTION('ref_axis',(0.,0.,1.)) ;
#2718=DIRECTION('center_axis',(-1.,0.,0.)) ;
#2719=DIRECTION('ref_axis',(0.,0.,1.)) ;
#2720=DIRECTION('center_axis',(-1.,0.,0.)) ;
#2721=DIRECTION('ref_axis',(0.,0.,1.)) ;
#2722=DIRECTION('',(1.,0.,0.)) ;
#2723=DIRECTION('center_axis',(1.,0.,0.)) ;
#2724=DIRECTION('ref_axis',(0.,0.,-1.)) ;
#2725=DIRECTION('center_axis',(-1.,0.,0.)) ;
#2726=DIRECTION('ref_axis',(0.,0.,1.)) ;
#2727=DIRECTION('center_axis',(-1.,0.,0.)) ;
#2728=DIRECTION('ref_axis',(0.,0.,1.)) ;
#2729=DIRECTION('',(0.707106781186553,8.65956056235487E-17,0.707106781186542)) ;
#2730=DIRECTION('center_axis',(-1.,0.,0.)) ;
#2731=DIRECTION('ref_axis',(0.,0.,1.)) ;
#2732=DIRECTION('center_axis',(-1.,0.,0.)) ;
#2733=DIRECTION('ref_axis',(0.,0.,1.)) ;
#2734=DIRECTION('',(1.,0.,0.)) ;
#2735=DIRECTION('center_axis',(1.,0.,0.)) ;
#2736=DIRECTION('ref_axis',(0.,0.,-1.)) ;
#2737=DIRECTION('center_axis',(-1.,0.,0.)) ;
#2738=DIRECTION('ref_axis',(0.,0.,1.)) ;
#2739=DIRECTION('center_axis',(1.,0.,0.)) ;
#2740=DIRECTION('ref_axis',(0.,0.,-1.)) ;
#2741=DIRECTION('',(0.,0.500000000000002,0.866025403784438)) ;
#2742=DIRECTION('',(0.,1.,2.3112532288264E-16)) ;
#2743=DIRECTION('center_axis',(1.,0.,0.)) ;
#2744=DIRECTION('ref_axis',(0.,0.,-1.)) ;
#2745=DIRECTION('',(0.,0.500000000000002,0.866025403784438)) ;
#2746=DIRECTION('',(0.,-0.5,0.866025403784438)) ;
#2747=DIRECTION('center_axis',(1.,0.,0.)) ;
#2748=DIRECTION('ref_axis',(0.,0.,-1.)) ;
#2749=DIRECTION('',(0.,-0.5,0.866025403784438)) ;
#2750=DIRECTION('',(0.,-1.,2.3112532288264E-16)) ;
#2751=DIRECTION('center_axis',(1.,0.,0.)) ;
#2752=DIRECTION('ref_axis',(0.,0.,-1.)) ;
#2753=DIRECTION('',(0.,-1.,2.3112532288264E-16)) ;
#2754=DIRECTION('',(0.,-0.500000000000002,-0.866025403784438)) ;
#2755=DIRECTION('center_axis',(1.,0.,0.)) ;
#2756=DIRECTION('ref_axis',(0.,0.,-1.)) ;
#2757=DIRECTION('',(0.,-0.500000000000002,-0.866025403784438)) ;
#2758=DIRECTION('',(0.,0.499999999999999,-0.866025403784439)) ;
#2759=DIRECTION('center_axis',(1.,0.,0.)) ;
#2760=DIRECTION('ref_axis',(0.,0.,-1.)) ;
#2761=DIRECTION('',(0.,0.499999999999999,-0.866025403784439)) ;
#2762=DIRECTION('',(0.,1.,2.3112532288264E-16)) ;
#2763=DIRECTION('center_axis',(1.,0.,0.)) ;
#2764=DIRECTION('ref_axis',(0.,0.,-1.)) ;
#2765=DIRECTION('center_axis',(1.,0.,0.)) ;
#2766=DIRECTION('ref_axis',(0.,0.,-1.)) ;
#2767=DIRECTION('center_axis',(1.,0.,0.)) ;
#2768=DIRECTION('ref_axis',(0.,0.,-1.)) ;
#2769=DIRECTION('center_axis',(1.,0.,0.)) ;
#2770=DIRECTION('ref_axis',(0.,0.,-1.)) ;
#2771=DIRECTION('center_axis',(1.,0.,0.)) ;
#2772=DIRECTION('ref_axis',(0.,0.,-1.)) ;
#2773=DIRECTION('center_axis',(-1.,0.,0.)) ;
#2774=DIRECTION('ref_axis',(0.,0.,1.)) ;
#2775=DIRECTION('center_axis',(1.,0.,0.)) ;
#2776=DIRECTION('ref_axis',(0.,0.,-1.)) ;
#2777=DIRECTION('center_axis',(1.,0.,0.)) ;
#2778=DIRECTION('ref_axis',(0.,0.,-1.)) ;
#2779=DIRECTION('center_axis',(1.,0.,0.)) ;
#2780=DIRECTION('ref_axis',(0.,0.,-1.)) ;
#2781=DIRECTION('center_axis',(1.,0.,0.)) ;
#2782=DIRECTION('ref_axis',(0.,0.,-1.)) ;
#2783=DIRECTION('center_axis',(1.,0.,0.)) ;
#2784=DIRECTION('ref_axis',(0.,0.,-1.)) ;
#2785=DIRECTION('center_axis',(1.,0.,0.)) ;
#2786=DIRECTION('ref_axis',(0.,0.,-1.)) ;
#2787=DIRECTION('center_axis',(1.,0.,0.)) ;
#2788=DIRECTION('ref_axis',(0.,0.,-1.)) ;
#2789=DIRECTION('center_axis',(0.,-2.3112532288264E-16,1.)) ;
#2790=DIRECTION('ref_axis',(0.,-1.,-2.3112532288264E-16)) ;
#2791=DIRECTION('',(-1.,0.,0.)) ;
#2792=DIRECTION('',(-1.,0.,0.)) ;
#2793=DIRECTION('center_axis',(0.,0.866025403784439,0.499999999999999)) ;
#2794=DIRECTION('ref_axis',(0.,-0.499999999999999,0.866025403784439)) ;
#2795=DIRECTION('',(-1.,0.,0.)) ;
#2796=DIRECTION('center_axis',(0.,0.866025403784438,-0.500000000000002)) ;
#2797=DIRECTION('ref_axis',(0.,0.500000000000002,0.866025403784438)) ;
#2798=DIRECTION('',(-1.,0.,0.)) ;
#2799=DIRECTION('center_axis',(0.,-2.3112532288264E-16,-1.)) ;
#2800=DIRECTION('ref_axis',(0.,1.,-2.3112532288264E-16)) ;
#2801=DIRECTION('',(-1.,0.,0.)) ;
#2802=DIRECTION('center_axis',(0.,-0.866025403784438,-0.5)) ;
#2803=DIRECTION('ref_axis',(0.,0.5,-0.866025403784438)) ;
#2804=DIRECTION('',(-1.,0.,0.)) ;
#2805=DIRECTION('center_axis',(0.,-0.866025403784438,0.500000000000002)) ;
#2806=DIRECTION('ref_axis',(0.,-0.500000000000002,-0.866025403784438)) ;
#3300=CARTESIAN_POINT('',(0.,0.,0.)) ;
#3301=CARTESIAN_POINT('Origin',(5.7,0.,0.)) ;
#3302=CARTESIAN_POINT('',(5.7,4.89858719658941E-16,-4.)) ;
#3303=CARTESIAN_POINT('',(5.7,-4.89858719658941E-16,4.)) ;
#3304=CARTESIAN_POINT('Origin',(5.7,0.,0.)) ;
#3305=CARTESIAN_POINT('Origin',(5.7,0.,0.)) ;
#3306=CARTESIAN_POINT('',(5.3,-5.38844591624835E-16,4.4)) ;
#3307=CARTESIAN_POINT('Origin',(5.7,-5.38844591624835E-16,4.4)) ;
#3308=CARTESIAN_POINT('Origin',(5.3,0.,0.)) ;
#3309=CARTESIAN_POINT('Origin',(0.,0.,0.)) ;
#3310=CARTESIAN_POINT('',(4.7,5.62916512459884,-3.25000000000001)) ;
#3311=CARTESIAN_POINT('',(4.7,1.50231459873716E-15,-6.5)) ;
#3312=CARTESIAN_POINT('Origin',(4.7,0.,0.)) ;
#3313=CARTESIAN_POINT('',(4.7,5.62916512459885,3.25)) ;
#3314=CARTESIAN_POINT('Origin',(4.7,0.,0.)) ;
#3315=CARTESIAN_POINT('',(4.7,0.,6.5)) ;
#3316=CARTESIAN_POINT('Origin',(4.7,0.,0.)) ;
#3317=CARTESIAN_POINT('',(4.7,-5.62916512459884,3.25000000000001)) ;
#3318=CARTESIAN_POINT('Origin',(4.7,0.,0.)) ;
#3319=CARTESIAN_POINT('',(4.7,-5.62916512459885,-3.25)) ;
#3320=CARTESIAN_POINT('Origin',(4.7,0.,0.)) ;
#3321=CARTESIAN_POINT('Origin',(4.7,0.,0.)) ;
#3322=CARTESIAN_POINT('',(5.3,-7.96020419445779E-16,-6.5)) ;
#3323=CARTESIAN_POINT('',(0.,-7.9602041944578E-16,-6.5)) ;
#3324=CARTESIAN_POINT('Origin',(5.3,0.,0.)) ;
#3325=CARTESIAN_POINT('Origin',(40.3,0.,0.)) ;
#3326=CARTESIAN_POINT('',(39.6095,-4.89858719658941E-16,-4.)) ;
#3327=CARTESIAN_POINT('Origin',(39.6095,0.,0.)) ;
#3328=CARTESIAN_POINT('',(40.3,-4.05296858177817E-16,-3.3095)) ;
#3329=CARTESIAN_POINT('',(40.3,-4.05296858177817E-16,-3.3095)) ;
#3330=CARTESIAN_POINT('Origin',(40.3,0.,0.)) ;
#3331=CARTESIAN_POINT('Origin',(0.,0.,0.)) ;
#3332=CARTESIAN_POINT('',(0.,-4.89858719658941E-16,-4.)) ;
#3333=CARTESIAN_POINT('Origin',(5.3,7.50555349946514,-6.50521303491302E-16)) ;
#3334=CARTESIAN_POINT('Origin',(40.3,0.,0.)) ;
#3335=CARTESIAN_POINT('Origin',(4.7,6.5,0.)) ;
#3336=CARTESIAN_POINT('',(4.7,3.75277674973255,-6.5)) ;
#3337=CARTESIAN_POINT('',(4.7,3.75277674973255,-6.5)) ;
#3338=CARTESIAN_POINT('',(4.7,3.75277674973255,-6.5)) ;
#3339=CARTESIAN_POINT('Origin',(4.7,6.5,0.)) ;
#3340=CARTESIAN_POINT('',(4.7,7.50555349946514,0.)) ;
#3341=CARTESIAN_POINT('',(4.7,3.75277674973255,-6.5)) ;
#3342=CARTESIAN_POINT('',(4.7,7.50555349946514,0.)) ;
#3343=CARTESIAN_POINT('Origin',(4.7,6.5,0.)) ;
#3344=CARTESIAN_POINT('',(4.7,3.75277674973257,6.5)) ;
#3345=CARTESIAN_POINT('',(4.7,7.50555349946514,0.)) ;
#3346=CARTESIAN_POINT('',(4.7,3.75277674973257,6.5)) ;
#3347=CARTESIAN_POINT('Origin',(4.7,6.5,0.)) ;
#3348=CARTESIAN_POINT('',(4.7,-3.75277674973255,6.5)) ;
#3349=CARTESIAN_POINT('',(4.7,3.75277674973257,6.5)) ;
#3350=CARTESIAN_POINT('',(4.7,-7.50555349946514,3.54642105489778E-16)) ;
#3351=CARTESIAN_POINT('Origin',(4.7,6.5,0.)) ;
#3352=CARTESIAN_POINT('',(4.7,-7.50555349946514,0.)) ;
#3353=CARTESIAN_POINT('',(4.7,-7.50555349946514,3.54642105489778E-16)) ;
#3354=CARTESIAN_POINT('',(4.7,-3.75277674973258,-6.5)) ;
#3355=CARTESIAN_POINT('Origin',(4.7,6.5,0.)) ;
#3356=CARTESIAN_POINT('',(4.7,-3.75277674973258,-6.5)) ;
#3357=CARTESIAN_POINT('',(4.7,-3.75277674973258,-6.5)) ;
#3358=CARTESIAN_POINT('',(4.7,3.75277674973255,-6.5)) ;
#3359=CARTESIAN_POINT('Origin',(0.,7.50555349946514,-6.50521303491302E-16)) ;
#3360=CARTESIAN_POINT('',(0.,1.50231459873716E-15,-6.5)) ;
#3361=CARTESIAN_POINT('',(0.,5.62916512459884,-3.25000000000001)) ;
#3362=CARTESIAN_POINT('Origin',(0.,0.,0.)) ;
#3363=CARTESIAN_POINT('',(0.,-5.62916512459885,-3.24999999999999)) ;
#3364=CARTESIAN_POINT('Origin',(0.,0.,0.)) ;
#3365=CARTESIAN_POINT('',(0.,-5.62916512459884,3.25000000000001)) ;
#3366=CARTESIAN_POINT('Origin',(0.,0.,0.)) ;
#3367=CARTESIAN_POINT('',(0.,1.50231459873716E-15,6.5)) ;
#3368=CARTESIAN_POINT('Origin',(0.,0.,0.)) ;
#3369=CARTESIAN_POINT('',(0.,5.62916512459885,3.25)) ;
#3370=CARTESIAN_POINT('Origin',(0.,0.,0.)) ;
#3371=CARTESIAN_POINT('Origin',(0.,0.,0.)) ;
#3372=CARTESIAN_POINT('Origin',(0.,0.,0.)) ;
#3373=CARTESIAN_POINT('',(0.580556583600765,7.50555349946514,1.86597838430726E-16)) ;
#3374=CARTESIAN_POINT('Ctrl Pts',(2.52404060397759E-15,5.62916512459885,
3.25000000000001)) ;
#3375=CARTESIAN_POINT('Ctrl Pts',(1.94289029309402E-15,6.50000000000069,
1.7416697508011)) ;
#3376=CARTESIAN_POINT('Ctrl Pts',(0.58055658360176,7.50555349946686,-2.98168594117076E-12)) ;
#3377=CARTESIAN_POINT('Ctrl Pts',(0.58055658360176,7.50555349946686,2.98331750666524E-12)) ;
#3378=CARTESIAN_POINT('Ctrl Pts',(-1.12537942179479E-15,6.50000000000069,
-1.7416697508011)) ;
#3379=CARTESIAN_POINT('Ctrl Pts',(-1.13581827178992E-15,5.62916512459884,
-3.25000000000001)) ;
#3380=CARTESIAN_POINT('Origin',(0.,0.,0.)) ;
#3381=CARTESIAN_POINT('',(0.580556583600762,3.75277674973257,6.5)) ;
#3382=CARTESIAN_POINT('Ctrl Pts',(1.13581827178992E-15,2.52404060397759E-15,
6.5)) ;
#3383=CARTESIAN_POINT('Ctrl Pts',(1.2490009027033E-15,1.74166975080368,
6.5)) ;
#3384=CARTESIAN_POINT('Ctrl Pts',(0.580556583601757,3.75277674973601,6.5)) ;
#3385=CARTESIAN_POINT('Ctrl Pts',(0.580556583601759,3.75277674973085,6.50000000000299)) ;
#3386=CARTESIAN_POINT('Ctrl Pts',(3.30581563765696E-15,4.75833024919701,
4.75833024919891)) ;
#3387=CARTESIAN_POINT('Ctrl Pts',(2.52404060397759E-15,5.62916512459885,
3.25000000000001)) ;
#3388=CARTESIAN_POINT('Origin',(0.,0.,0.)) ;
#3389=CARTESIAN_POINT('',(0.580556583600758,-3.75277674973255,6.5)) ;
#3390=CARTESIAN_POINT('Ctrl Pts',(0.580556583601755,-3.752776749736,6.5)) ;
#3391=CARTESIAN_POINT('Ctrl Pts',(1.12537942179479E-15,-1.74166975080368,
6.5)) ;
#3392=CARTESIAN_POINT('Ctrl Pts',(1.13581827178992E-15,2.52404060397759E-15,
6.5)) ;
#3393=CARTESIAN_POINT('Ctrl Pts',(0.,-5.62916512459884,3.25000000000001)) ;
#3394=CARTESIAN_POINT('Ctrl Pts',(2.77555756156289E-16,-4.758330249197,
4.75833024919891)) ;
#3395=CARTESIAN_POINT('Ctrl Pts',(0.580556583601755,-3.75277674973083,6.50000000000299)) ;
#3396=CARTESIAN_POINT('Origin',(0.,0.,0.)) ;
#3397=CARTESIAN_POINT('',(0.580556583600765,-7.50555349946514,-1.19038851851474E-16)) ;
#3398=CARTESIAN_POINT('Ctrl Pts',(0.580556583601757,-7.50555349946686,-2.97026498270936E-12)) ;
#3399=CARTESIAN_POINT('Ctrl Pts',(0.,-6.50000000000069,1.74166975080111)) ;
#3400=CARTESIAN_POINT('Ctrl Pts',(0.,-5.62916512459884,3.25000000000001)) ;
#3401=CARTESIAN_POINT('Ctrl Pts',(5.42668729855182E-15,-5.62916512459886,
-3.25)) ;
#3402=CARTESIAN_POINT('Ctrl Pts',(4.92661467177413E-15,-6.5000000000007,
-1.7416697508011)) ;
#3403=CARTESIAN_POINT('Ctrl Pts',(0.58055658360176,-7.50555349946686,2.97923859292903E-12)) ;
#3404=CARTESIAN_POINT('Origin',(0.,0.,0.)) ;
#3405=CARTESIAN_POINT('',(0.580556583600758,3.75277674973255,-6.5)) ;
#3406=CARTESIAN_POINT('Ctrl Pts',(-1.13581827178992E-15,5.62916512459884,
-3.25000000000001)) ;
#3407=CARTESIAN_POINT('Ctrl Pts',(-1.04083408558608E-15,4.758330249197,
-4.75833024919891)) ;
#3408=CARTESIAN_POINT('Ctrl Pts',(0.580556583601754,3.75277674973083,-6.50000000000299)) ;
#3409=CARTESIAN_POINT('Ctrl Pts',(0.58055658360175,3.75277674973599,-6.5)) ;
#3410=CARTESIAN_POINT('Ctrl Pts',(3.103447877054E-16,1.74166975080367,-6.5)) ;
#3411=CARTESIAN_POINT('Ctrl Pts',(1.13581827178992E-15,-2.01923248318207E-15,
-6.5)) ;
#3412=CARTESIAN_POINT('Origin',(0.,0.,0.)) ;
#3413=CARTESIAN_POINT('',(0.580556583600767,-3.75277674973258,-6.5)) ;
#3414=CARTESIAN_POINT('Ctrl Pts',(0.580556583601764,-3.75277674973085,-6.50000000000299)) ;
#3415=CARTESIAN_POINT('Ctrl Pts',(6.02079077550993E-15,-4.75833024919702,
-4.75833024919891)) ;
#3416=CARTESIAN_POINT('Ctrl Pts',(5.42668729855182E-15,-5.62916512459886,
-3.25)) ;
#3417=CARTESIAN_POINT('Ctrl Pts',(1.13581827178992E-15,-2.01923248318207E-15,
-6.5)) ;
#3418=CARTESIAN_POINT('Ctrl Pts',(2.15105711021124E-15,-1.74166975080369,
-6.5)) ;
#3419=CARTESIAN_POINT('Ctrl Pts',(0.580556583601762,-3.75277674973603,-6.5)) ;
#3420=CARTESIAN_POINT('Origin',(5.3,3.75277674973255,-6.5)) ;
#3421=CARTESIAN_POINT('',(5.3,-3.75277674973258,-6.5)) ;
#3422=CARTESIAN_POINT('',(5.3,3.75277674973255,-6.5)) ;
#3423=CARTESIAN_POINT('Origin',(5.3,-3.75277674973258,-6.5)) ;
#3424=CARTESIAN_POINT('',(5.3,-7.50555349946514,3.54642105489778E-16)) ;
#3425=CARTESIAN_POINT('Origin',(5.3,-7.50555349946514,3.54642105489778E-16)) ;
#3426=CARTESIAN_POINT('',(5.3,-3.75277674973255,6.5)) ;
#3427=CARTESIAN_POINT('Origin',(5.3,3.75277674973257,6.5)) ;
#3428=CARTESIAN_POINT('',(5.3,3.75277674973257,6.5)) ;
#3429=CARTESIAN_POINT('Origin',(5.3,7.50555349946514,0.)) ;
#3430=CARTESIAN_POINT('',(5.3,7.50555349946514,0.)) ;
#3431=CARTESIAN_POINT('Origin',(5.3,3.75277674973255,-6.5)) ;
#3456=UNCERTAINTY_MEASURE_WITH_UNIT(LENGTH_MEASURE(0.01),#3476,
'DISTANCE_ACCURACY_VALUE',
'Maximum model space distance between geometric entities at asserted c
onnectivities') ;
#3457=UNCERTAINTY_MEASURE_WITH_UNIT(LENGTH_MEASURE(0.01),#3476,
'DISTANCE_ACCURACY_VALUE',
'Maximum model space distance between geometric entities at asserted c
onnectivities') ;
#3474=(
GEOMETRIC_REPRESENTATION_CONTEXT(3)
GLOBAL_UNCERTAINTY_ASSIGNED_CONTEXT((#3456))
GLOBAL_UNIT_ASSIGNED_CONTEXT((#3476,#3478,#3479))
REPRESENTATION_CONTEXT('','3D')
) ;
#3475=(
GEOMETRIC_REPRESENTATION_CONTEXT(3)
GLOBAL_UNCERTAINTY_ASSIGNED_CONTEXT((#3457))
GLOBAL_UNIT_ASSIGNED_CONTEXT((#3476,#3478,#3479))
REPRESENTATION_CONTEXT('','3D')
) ;
#3476=(
LENGTH_UNIT()
NAMED_UNIT(*)
SI_UNIT(.MILLI.,.METRE.)
) ;
#3478=(
NAMED_UNIT(*)
PLANE_ANGLE_UNIT()
SI_UNIT($,.RADIAN.)
) ;
#3479=(
NAMED_UNIT(*)
SI_UNIT($,.STERADIAN.)
SOLID_ANGLE_UNIT()
) ;
#3496=SHAPE_DEFINITION_REPRESENTATION(#3529,#3554) ;
#3529=PRODUCT_DEFINITION_SHAPE('',$,#3572) ;
#3554=SHAPE_REPRESENTATION('',(#2161),#3474) ;
#3555=PRODUCT_DEFINITION_CONTEXT('part definition',#3608,'design') ;
#3572=PRODUCT_DEFINITION('Hex_Screw_M8x35',
'Hex_Screw_M8x35',#3589,#3555) ;
#3589=PRODUCT_DEFINITION_FORMATION('',$,#3626) ;
#3608=APPLICATION_CONTEXT(
'Core Data for Automotive Mechanical Design Process') ;
#3609=PRODUCT_CONTEXT('part definition',#3608,'mechanical') ;
#3626=PRODUCT('Hex_Screw_M8x35',
'Hex_Screw_M8x35',$,(#3609)) ;
#3628=PRESENTATION_STYLE_ASSIGNMENT((#3630)) ;
#3630=SURFACE_STYLE_USAGE(.BOTH.,#3632) ;
#3632=SURFACE_SIDE_STYLE('',(#3634)) ;
#3634=SURFACE_STYLE_FILL_AREA(#3636) ;
#3636=FILL_AREA_STYLE('Opaque(202,209,238)',(#3638)) ;
#3638=FILL_AREA_STYLE_COLOUR('Opaque(202,209,238)',#3640) ;
#3640=COLOUR_RGB('Opaque(202,209,238)', 0.09019608, 0.27058824, 0.51372549) ;
ENDSEC;
END-ISO-10303-21;
